ISO-10303-21;
HEADER;
/* Generated by software containing ST-Developer
 * from STEP Tools, Inc. (www.steptools.com) 
 */

FILE_DESCRIPTION(
/* description */ ('Worm-less right-angle friction wheel drive'),
/* implementation_level */ '2;1');

FILE_NAME(
/* name */ 'Output collar (1).step',
/* time_stamp */ '2026-10-28T03:22:36-07:00',
/* author */ (''),
/* organization */ (''),
/* preprocessor_version */ 'ST-DEVELOPER v20.2',
/* originating_system */ 'Autodesk Translation Framework v15.17.0.0',
/* authorisation */ '');

FILE_SCHEMA (('AUTOMOTIVE_DESIGN { 1 0 10303 214 3 1 1 }'));
ENDSEC;

DATA;
#10=MECHANICAL_DESIGN_GEOMETRIC_PRESENTATION_REPRESENTATION('',(#662),#17046);
#508=B_SPLINE_CURVE_WITH_KNOTS('',3,(#16732,#16733,#16734,#16735,#16736,
#16737),.UNSPECIFIED.,.F.,.F.,(4,2,4),(0.818088904349171,0.878131747417164,
0.957937926194035),.UNSPECIFIED.);
#509=B_SPLINE_CURVE_WITH_KNOTS('',3,(#16741,#16742,#16743,#16744,#16745,
#16746),.UNSPECIFIED.,.F.,.F.,(4,2,4),(0.319312642064678,0.399118820841549,
0.459161663909542),.UNSPECIFIED.);
#510=B_SPLINE_CURVE_WITH_KNOTS('',3,(#16747,#16748,#16749,#16750,#16751,
#16752),.UNSPECIFIED.,.F.,.F.,(4,2,4),(0.179463620219812,0.239506463287808,
0.319312642064678),.UNSPECIFIED.);
#511=B_SPLINE_CURVE_WITH_KNOTS('',3,(#16753,#16754,#16755,#16756,#16757,
#16758),.UNSPECIFIED.,.F.,.F.,(4,2,4),(0.957937926194035,1.03774410497091,
1.0977869480389),.UNSPECIFIED.);
#512=B_SPLINE_CURVE_WITH_KNOTS('',3,(#16762,#16763,#16764,#16765,#16766,
#16767,#16768,#16769,#16770,#16771),.UNSPECIFIED.,.F.,.F.,(4,2,2,2,4),(0.,
0.0793157643915219,0.158631528783044,0.23794361593365,0.317255703084255),
 .UNSPECIFIED.);
#513=B_SPLINE_CURVE_WITH_KNOTS('',3,(#16773,#16774,#16775,#16776,#16777,
#16778,#16779,#16780,#16781,#16782),.UNSPECIFIED.,.F.,.F.,(4,2,2,2,4),(0.951767109252766,
1.03107919640337,1.11039128355398,1.1897070479455,1.26902281233702),
 .UNSPECIFIED.);
#514=B_SPLINE_CURVE_WITH_KNOTS('',3,(#16783,#16784,#16785,#16786,#16787,
#16788,#16789,#16790,#16791,#16792,#16793,#16794,#16795,#16796,#16797,#16798,
#16799,#16800),.UNSPECIFIED.,.F.,.F.,(4,2,2,2,2,2,2,2,4),(0.317255703084255,
0.396567790234861,0.475879877385467,0.555195641776989,0.634511406168511,
0.713827170560032,0.793142934951554,0.87245502210216,0.951767109252766),
 .UNSPECIFIED.);
#561=SHAPE_REPRESENTATION_RELATIONSHIP('SRR','None',#17307,#608);
#608=ADVANCED_BREP_SHAPE_REPRESENTATION('',(#712),#17043);
#662=STYLED_ITEM('',(#17605),#712);
#712=MANIFOLD_SOLID_BREP('Body1',#8221);
#949=FACE_BOUND('',#2352,.T.);
#950=FACE_BOUND('',#2354,.T.);
#1185=PLANE('',#9713);
#1186=PLANE('',#9717);
#1187=PLANE('',#9724);
#1188=PLANE('',#9725);
#1646=FACE_OUTER_BOUND('',#2346,.T.);
#1647=FACE_OUTER_BOUND('',#2347,.T.);
#1648=FACE_OUTER_BOUND('',#2348,.T.);
#1649=FACE_OUTER_BOUND('',#2349,.T.);
#1650=FACE_OUTER_BOUND('',#2350,.T.);
#1651=FACE_OUTER_BOUND('',#2351,.T.);
#1652=FACE_OUTER_BOUND('',#2353,.T.);
#2346=EDGE_LOOP('',(#7396,#7397));
#2347=EDGE_LOOP('',(#7398,#7399,#7400,#7401,#7402,#7403,#7404,#7405,#7406,
#7407,#7408));
#2348=EDGE_LOOP('',(#7409,#7410));
#2349=EDGE_LOOP('',(#7411,#7412,#7413,#7414,#7415,#7416,#7417,#7418,#7419,
#7420,#7421,#7422));
#2350=EDGE_LOOP('',(#7423,#7424,#7425,#7426,#7427,#7428,#7429,#7430,#7431));
#2351=EDGE_LOOP('',(#7432));
#2352=EDGE_LOOP('',(#7433));
#2353=EDGE_LOOP('',(#7434));
#2354=EDGE_LOOP('',(#7435));
#2866=LINE('',#16727,#3406);
#2867=LINE('',#16760,#3407);
#2868=LINE('',#16802,#3408);
#2869=LINE('',#16806,#3409);
#2870=LINE('',#16808,#3410);
#2871=LINE('',#16813,#3411);
#2872=LINE('',#16815,#3412);
#3406=VECTOR('',#12206,1.);
#3407=VECTOR('',#12213,0.21);
#3408=VECTOR('',#12216,1.);
#3409=VECTOR('',#12221,0.605);
#3410=VECTOR('',#12222,0.605);
#3411=VECTOR('',#12229,1.1);
#3412=VECTOR('',#12230,1.1);
#3860=CIRCLE('',#9714,0.21);
#3861=CIRCLE('',#9716,0.21);
#3862=CIRCLE('',#9719,0.605);
#3863=CIRCLE('',#9720,0.605);
#3864=CIRCLE('',#9722,1.1);
#3865=CIRCLE('',#9723,1.1);
#4492=VERTEX_POINT('',#16725);
#4493=VERTEX_POINT('',#16726);
#4494=VERTEX_POINT('',#16730);
#4495=VERTEX_POINT('',#16731);
#4496=VERTEX_POINT('',#16738);
#4497=VERTEX_POINT('',#16740);
#4498=VERTEX_POINT('',#16759);
#4499=VERTEX_POINT('',#16761);
#4500=VERTEX_POINT('',#16772);
#4501=VERTEX_POINT('',#16804);
#4502=VERTEX_POINT('',#16807);
#4503=VERTEX_POINT('',#16811);
#4504=VERTEX_POINT('',#16814);
#5467=EDGE_CURVE('',#4492,#4493,#2866,.T.);
#5468=EDGE_CURVE('',#4492,#4493,#3860,.T.);
#5469=EDGE_CURVE('',#4494,#4495,#508,.T.);
#5470=EDGE_CURVE('',#4496,#4494,#3861,.T.);
#5471=EDGE_CURVE('',#4497,#4496,#509,.T.);
#5472=EDGE_CURVE('',#4493,#4497,#510,.T.);
#5473=EDGE_CURVE('',#4495,#4492,#511,.T.);
#5474=EDGE_CURVE('',#4495,#4498,#2867,.T.);
#5475=EDGE_CURVE('',#4499,#4498,#512,.T.);
#5476=EDGE_CURVE('',#4500,#4499,#513,.T.);
#5477=EDGE_CURVE('',#4498,#4500,#514,.T.);
#5478=EDGE_CURVE('',#4496,#4494,#2868,.T.);
#5479=EDGE_CURVE('',#4501,#4501,#3862,.T.);
#5480=EDGE_CURVE('',#4501,#4497,#2869,.T.);
#5481=EDGE_CURVE('',#4495,#4502,#2870,.T.);
#5482=EDGE_CURVE('',#4502,#4502,#3863,.T.);
#5483=EDGE_CURVE('',#4503,#4503,#3864,.T.);
#5484=EDGE_CURVE('',#4503,#4500,#2871,.T.);
#5485=EDGE_CURVE('',#4498,#4504,#2872,.T.);
#5486=EDGE_CURVE('',#4504,#4504,#3865,.T.);
#7396=ORIENTED_EDGE('',*,*,#5467,.F.);
#7397=ORIENTED_EDGE('',*,*,#5468,.T.);
#7398=ORIENTED_EDGE('',*,*,#5469,.F.);
#7399=ORIENTED_EDGE('',*,*,#5470,.F.);
#7400=ORIENTED_EDGE('',*,*,#5471,.F.);
#7401=ORIENTED_EDGE('',*,*,#5472,.F.);
#7402=ORIENTED_EDGE('',*,*,#5468,.F.);
#7403=ORIENTED_EDGE('',*,*,#5473,.F.);
#7404=ORIENTED_EDGE('',*,*,#5474,.T.);
#7405=ORIENTED_EDGE('',*,*,#5475,.F.);
#7406=ORIENTED_EDGE('',*,*,#5476,.F.);
#7407=ORIENTED_EDGE('',*,*,#5477,.F.);
#7408=ORIENTED_EDGE('',*,*,#5474,.F.);
#7409=ORIENTED_EDGE('',*,*,#5478,.F.);
#7410=ORIENTED_EDGE('',*,*,#5470,.T.);
#7411=ORIENTED_EDGE('',*,*,#5479,.F.);
#7412=ORIENTED_EDGE('',*,*,#5480,.T.);
#7413=ORIENTED_EDGE('',*,*,#5471,.T.);
#7414=ORIENTED_EDGE('',*,*,#5478,.T.);
#7415=ORIENTED_EDGE('',*,*,#5469,.T.);
#7416=ORIENTED_EDGE('',*,*,#5481,.T.);
#7417=ORIENTED_EDGE('',*,*,#5482,.T.);
#7418=ORIENTED_EDGE('',*,*,#5481,.F.);
#7419=ORIENTED_EDGE('',*,*,#5473,.T.);
#7420=ORIENTED_EDGE('',*,*,#5467,.T.);
#7421=ORIENTED_EDGE('',*,*,#5472,.T.);
#7422=ORIENTED_EDGE('',*,*,#5480,.F.);
#7423=ORIENTED_EDGE('',*,*,#5483,.F.);
#7424=ORIENTED_EDGE('',*,*,#5484,.T.);
#7425=ORIENTED_EDGE('',*,*,#5476,.T.);
#7426=ORIENTED_EDGE('',*,*,#5475,.T.);
#7427=ORIENTED_EDGE('',*,*,#5485,.T.);
#7428=ORIENTED_EDGE('',*,*,#5486,.T.);
#7429=ORIENTED_EDGE('',*,*,#5485,.F.);
#7430=ORIENTED_EDGE('',*,*,#5477,.T.);
#7431=ORIENTED_EDGE('',*,*,#5484,.F.);
#7432=ORIENTED_EDGE('',*,*,#5483,.T.);
#7433=ORIENTED_EDGE('',*,*,#5479,.T.);
#7434=ORIENTED_EDGE('',*,*,#5486,.F.);
#7435=ORIENTED_EDGE('',*,*,#5482,.F.);
#7696=CYLINDRICAL_SURFACE('',#9715,0.21);
#7697=CYLINDRICAL_SURFACE('',#9718,0.605);
#7698=CYLINDRICAL_SURFACE('',#9721,1.1);
#8138=ADVANCED_FACE('',(#1646),#1185,.T.);
#8139=ADVANCED_FACE('',(#1647),#7696,.F.);
#8140=ADVANCED_FACE('',(#1648),#1186,.T.);
#8141=ADVANCED_FACE('',(#1649),#7697,.F.);
#8142=ADVANCED_FACE('',(#1650),#7698,.T.);
#8143=ADVANCED_FACE('',(#1651,#949),#1187,.T.);
#8144=ADVANCED_FACE('',(#1652,#950),#1188,.F.);
#8221=CLOSED_SHELL('',(#8138,#8139,#8140,#8141,#8142,#8143,#8144));
#9712=AXIS2_PLACEMENT_3D('',#16723,#12202,#12203);
#9713=AXIS2_PLACEMENT_3D('',#16724,#12204,#12205);
#9714=AXIS2_PLACEMENT_3D('',#16728,#12207,#12208);
#9715=AXIS2_PLACEMENT_3D('',#16729,#12209,#12210);
#9716=AXIS2_PLACEMENT_3D('',#16739,#12211,#12212);
#9717=AXIS2_PLACEMENT_3D('',#16801,#12214,#12215);
#9718=AXIS2_PLACEMENT_3D('',#16803,#12217,#12218);
#9719=AXIS2_PLACEMENT_3D('',#16805,#12219,#12220);
#9720=AXIS2_PLACEMENT_3D('',#16809,#12223,#12224);
#9721=AXIS2_PLACEMENT_3D('',#16810,#12225,#12226);
#9722=AXIS2_PLACEMENT_3D('',#16812,#12227,#12228);
#9723=AXIS2_PLACEMENT_3D('',#16816,#12231,#12232);
#9724=AXIS2_PLACEMENT_3D('',#16817,#12233,#12234);
#9725=AXIS2_PLACEMENT_3D('',#16818,#12235,#12236);
#12202=DIRECTION('axis',(0.,0.,1.));
#12203=DIRECTION('refdir',(1.,0.,0.));
#12204=DIRECTION('center_axis',(0.,0.,1.));
#12205=DIRECTION('ref_axis',(1.,0.,0.));
#12206=DIRECTION('',(1.,0.,0.));
#12207=DIRECTION('center_axis',(0.,0.,1.));
#12208=DIRECTION('ref_axis',(1.,0.,0.));
#12209=DIRECTION('center_axis',(0.,0.,1.));
#12210=DIRECTION('ref_axis',(1.,0.,0.));
#12211=DIRECTION('center_axis',(0.,0.,1.));
#12212=DIRECTION('ref_axis',(1.,0.,0.));
#12213=DIRECTION('',(0.,0.,1.));
#12214=DIRECTION('center_axis',(0.,0.,1.));
#12215=DIRECTION('ref_axis',(1.,0.,0.));
#12216=DIRECTION('',(-1.,0.,0.));
#12217=DIRECTION('center_axis',(1.,0.,0.));
#12218=DIRECTION('ref_axis',(0.,0.,-1.));
#12219=DIRECTION('center_axis',(-1.,0.,0.));
#12220=DIRECTION('ref_axis',(0.,0.,-1.));
#12221=DIRECTION('',(-1.,0.,0.));
#12222=DIRECTION('',(-1.,0.,0.));
#12223=DIRECTION('center_axis',(-1.,0.,0.));
#12224=DIRECTION('ref_axis',(0.,0.,-1.));
#12225=DIRECTION('center_axis',(1.,0.,0.));
#12226=DIRECTION('ref_axis',(0.,0.,-1.));
#12227=DIRECTION('center_axis',(1.,0.,0.));
#12228=DIRECTION('ref_axis',(0.,0.,-1.));
#12229=DIRECTION('',(-1.,0.,0.));
#12230=DIRECTION('',(-1.,0.,0.));
#12231=DIRECTION('center_axis',(1.,0.,0.));
#12232=DIRECTION('ref_axis',(0.,0.,-1.));
#12233=DIRECTION('center_axis',(1.,0.,0.));
#12234=DIRECTION('ref_axis',(0.,0.,-1.));
#12235=DIRECTION('center_axis',(1.,0.,0.));
#12236=DIRECTION('ref_axis',(0.,0.,-1.));
#16723=CARTESIAN_POINT('',(0.,0.,0.));
#16724=CARTESIAN_POINT('Origin',(6.4,3.,7.59));
#16725=CARTESIAN_POINT('',(6.23821310312636,2.86611572161004,7.59));
#16726=CARTESIAN_POINT('',(6.56178689687364,2.86611572161004,7.59));
#16727=CARTESIAN_POINT('',(6.,2.86611572161004,7.59));
#16728=CARTESIAN_POINT('Origin',(6.4,3.,7.59));
#16729=CARTESIAN_POINT('Origin',(6.4,3.,7.59));
#16730=CARTESIAN_POINT('',(6.23821310312636,3.13388427838996,7.59));
#16731=CARTESIAN_POINT('',(6.19,3.,7.605));
#16732=CARTESIAN_POINT('Ctrl Pts',(6.23821310312637,3.13388427838996,7.59));
#16733=CARTESIAN_POINT('Ctrl Pts',(6.22527883178237,3.1182543952608,7.59354677224418));
#16734=CARTESIAN_POINT('Ctrl Pts',(6.21420068341256,3.1001097876823,7.59698224789957));
#16735=CARTESIAN_POINT('Ctrl Pts',(6.19536143894557,3.05482987213252,7.6030741628997));
#16736=CARTESIAN_POINT('Ctrl Pts',(6.19,3.02660205959229,7.605));
#16737=CARTESIAN_POINT('Ctrl Pts',(6.19,3.,7.605));
#16738=CARTESIAN_POINT('',(6.56178689687364,3.13388427838996,7.59));
#16739=CARTESIAN_POINT('Origin',(6.4,3.,7.59));
#16740=CARTESIAN_POINT('',(6.61,3.,7.605));
#16741=CARTESIAN_POINT('Ctrl Pts',(6.61,3.,7.605));
#16742=CARTESIAN_POINT('Ctrl Pts',(6.61,3.02660205959229,7.605));
#16743=CARTESIAN_POINT('Ctrl Pts',(6.60463856105443,3.05482987213252,7.6030741628997));
#16744=CARTESIAN_POINT('Ctrl Pts',(6.58579931658744,3.1001097876823,7.59698224789957));
#16745=CARTESIAN_POINT('Ctrl Pts',(6.57472116821763,3.1182543952608,7.59354677224418));
#16746=CARTESIAN_POINT('Ctrl Pts',(6.56178689687364,3.13388427838996,7.59));
#16747=CARTESIAN_POINT('Ctrl Pts',(6.56178689687364,2.86611572161004,7.59));
#16748=CARTESIAN_POINT('Ctrl Pts',(6.57472116821763,2.8817456047392,7.59354677224418));
#16749=CARTESIAN_POINT('Ctrl Pts',(6.58579931658744,2.8998902123177,7.59698224789957));
#16750=CARTESIAN_POINT('Ctrl Pts',(6.60463856105443,2.94517012786748,7.6030741628997));
#16751=CARTESIAN_POINT('Ctrl Pts',(6.61,2.97339794040771,7.605));
#16752=CARTESIAN_POINT('Ctrl Pts',(6.61,3.,7.605));
#16753=CARTESIAN_POINT('Ctrl Pts',(6.19,3.,7.605));
#16754=CARTESIAN_POINT('Ctrl Pts',(6.19,2.97339794040771,7.605));
#16755=CARTESIAN_POINT('Ctrl Pts',(6.19536143894557,2.94517012786748,7.6030741628997));
#16756=CARTESIAN_POINT('Ctrl Pts',(6.21420068341256,2.8998902123177,7.59698224789957));
#16757=CARTESIAN_POINT('Ctrl Pts',(6.22527883178237,2.8817456047392,7.59354677224418));
#16758=CARTESIAN_POINT('Ctrl Pts',(6.23821310312636,2.86611572161004,7.59));
#16759=CARTESIAN_POINT('',(6.19,3.,8.1));
#16760=CARTESIAN_POINT('',(6.19,3.,7.59));
#16761=CARTESIAN_POINT('',(6.4,2.79,8.07976849370594));
#16762=CARTESIAN_POINT('Ctrl Pts',(6.4,2.79,8.07976849370594));
#16763=CARTESIAN_POINT('Ctrl Pts',(6.37356141186949,2.79,8.07976849370594));
#16764=CARTESIAN_POINT('Ctrl Pts',(6.34540621874507,2.79529707732902,8.08084015664674));
#16765=CARTESIAN_POINT('Ctrl Pts',(6.29368655445866,2.81674820319365,8.08468313707126));
#16766=CARTESIAN_POINT('Ctrl Pts',(6.27011632925886,2.83289882264279,8.08739593054622));
#16767=CARTESIAN_POINT('Ctrl Pts',(6.23289968538262,2.87011546651904,8.09246633289124));
#16768=CARTESIAN_POINT('Ctrl Pts',(6.21674838983659,2.89368605924271,8.09515738895358));
#16769=CARTESIAN_POINT('Ctrl Pts',(6.19529677343026,2.94540699667048,8.09895039220591));
#16770=CARTESIAN_POINT('Ctrl Pts',(6.19,2.97356263761647,8.1));
#16771=CARTESIAN_POINT('Ctrl Pts',(6.19,3.,8.1));
#16772=CARTESIAN_POINT('',(6.61,3.,8.1));
#16773=CARTESIAN_POINT('Ctrl Pts',(6.61,3.,8.1));
#16774=CARTESIAN_POINT('Ctrl Pts',(6.61,2.97356263761646,8.1));
#16775=CARTESIAN_POINT('Ctrl Pts',(6.60470322656974,2.94540699667048,8.09895039220591));
#16776=CARTESIAN_POINT('Ctrl Pts',(6.58325161016341,2.89368605924271,8.09515738895358));
#16777=CARTESIAN_POINT('Ctrl Pts',(6.56710031461738,2.87011546651904,8.09246633289124));
#16778=CARTESIAN_POINT('Ctrl Pts',(6.52988367074114,2.83289882264279,8.08739593054622));
#16779=CARTESIAN_POINT('Ctrl Pts',(6.50631344554134,2.81674820319365,8.08468313707126));
#16780=CARTESIAN_POINT('Ctrl Pts',(6.45459378125493,2.79529707732902,8.08084015664674));
#16781=CARTESIAN_POINT('Ctrl Pts',(6.42643858813051,2.79,8.07976849370594));
#16782=CARTESIAN_POINT('Ctrl Pts',(6.4,2.79,8.07976849370594));
#16783=CARTESIAN_POINT('Ctrl Pts',(6.19,3.,8.1));
#16784=CARTESIAN_POINT('Ctrl Pts',(6.19,3.02643736238353,8.1));
#16785=CARTESIAN_POINT('Ctrl Pts',(6.19529677343026,3.05459300332952,8.09895039220591));
#16786=CARTESIAN_POINT('Ctrl Pts',(6.21674838983659,3.10631394075729,8.09515738895358));
#16787=CARTESIAN_POINT('Ctrl Pts',(6.23289968538262,3.12988453348096,8.09246633289124));
#16788=CARTESIAN_POINT('Ctrl Pts',(6.27011632925886,3.16710117735721,8.08739593054622));
#16789=CARTESIAN_POINT('Ctrl Pts',(6.29368655445866,3.18325179680635,8.08468313707126));
#16790=CARTESIAN_POINT('Ctrl Pts',(6.34540621874507,3.20470292267098,8.08084015664674));
#16791=CARTESIAN_POINT('Ctrl Pts',(6.37356141186949,3.21,8.07976849370594));
#16792=CARTESIAN_POINT('Ctrl Pts',(6.42643858813051,3.21,8.07976849370594));
#16793=CARTESIAN_POINT('Ctrl Pts',(6.45459378125493,3.20470292267098,8.08084015664674));
#16794=CARTESIAN_POINT('Ctrl Pts',(6.50631344554134,3.18325179680635,8.08468313707126));
#16795=CARTESIAN_POINT('Ctrl Pts',(6.52988367074114,3.16710117735721,8.08739593054622));
#16796=CARTESIAN_POINT('Ctrl Pts',(6.56710031461738,3.12988453348096,8.09246633289124));
#16797=CARTESIAN_POINT('Ctrl Pts',(6.58325161016341,3.10631394075729,8.09515738895358));
#16798=CARTESIAN_POINT('Ctrl Pts',(6.60470322656974,3.05459300332952,8.09895039220591));
#16799=CARTESIAN_POINT('Ctrl Pts',(6.61,3.02643736238354,8.1));
#16800=CARTESIAN_POINT('Ctrl Pts',(6.61,3.,8.1));
#16801=CARTESIAN_POINT('Origin',(6.4,3.,7.59));
#16802=CARTESIAN_POINT('',(6.,3.13388427838996,7.59));
#16803=CARTESIAN_POINT('Origin',(6.,3.,7.));
#16804=CARTESIAN_POINT('',(6.8,3.,7.605));
#16805=CARTESIAN_POINT('Origin',(6.8,3.,7.));
#16806=CARTESIAN_POINT('',(6.,3.,7.605));
#16807=CARTESIAN_POINT('',(6.,3.,7.605));
#16808=CARTESIAN_POINT('',(6.,3.,7.605));
#16809=CARTESIAN_POINT('Origin',(6.,3.,7.));
#16810=CARTESIAN_POINT('Origin',(6.,3.,7.));
#16811=CARTESIAN_POINT('',(6.8,3.,8.1));
#16812=CARTESIAN_POINT('Origin',(6.8,3.,7.));
#16813=CARTESIAN_POINT('',(6.,3.,8.1));
#16814=CARTESIAN_POINT('',(6.,3.,8.1));
#16815=CARTESIAN_POINT('',(6.,3.,8.1));
#16816=CARTESIAN_POINT('Origin',(6.,3.,7.));
#16817=CARTESIAN_POINT('Origin',(6.8,3.,7.));
#16818=CARTESIAN_POINT('Origin',(6.,3.,7.));
#16990=UNCERTAINTY_MEASURE_WITH_UNIT(LENGTH_MEASURE(0.001),#17047,
'DISTANCE_ACCURACY_VALUE',
'Maximum model space distance between geometric entities at asserted c
onnectivities');
#16993=UNCERTAINTY_MEASURE_WITH_UNIT(LENGTH_MEASURE(0.001),#17047,
'DISTANCE_ACCURACY_VALUE',
'Maximum model space distance between geometric entities at asserted c
onnectivities');
#17043=(
GEOMETRIC_REPRESENTATION_CONTEXT(3)
GLOBAL_UNCERTAINTY_ASSIGNED_CONTEXT((#16990))
GLOBAL_UNIT_ASSIGNED_CONTEXT((#17047,#17049,#17050))
REPRESENTATION_CONTEXT('','3D')
);
#17046=(
GEOMETRIC_REPRESENTATION_CONTEXT(3)
GLOBAL_UNCERTAINTY_ASSIGNED_CONTEXT((#16993))
GLOBAL_UNIT_ASSIGNED_CONTEXT((#17047,#17049,#17050))
REPRESENTATION_CONTEXT('','3D')
);
#17047=(
LENGTH_UNIT()
NAMED_UNIT(*)
SI_UNIT(.CENTI.,.METRE.)
);
#17049=(
NAMED_UNIT(*)
PLANE_ANGLE_UNIT()
SI_UNIT($,.RADIAN.)
);
#17050=(
NAMED_UNIT(*)
SI_UNIT($,.STERADIAN.)
SOLID_ANGLE_UNIT()
);
#17100=SHAPE_DEFINITION_REPRESENTATION(#17234,#17307);
#17234=PRODUCT_DEFINITION_SHAPE('',$,#17360);
#17307=SHAPE_REPRESENTATION('',(#9712),#17043);
#17310=PRODUCT_DEFINITION_CONTEXT('part definition',#17468,'design');
#17360=PRODUCT_DEFINITION('Output collar (1)','Output collar (1)',#17412,
#17310);
#17412=PRODUCT_DEFINITION_FORMATION('',$,#17519);
#17468=APPLICATION_CONTEXT(
'Core Data for Automotive Mechanical Design Process');
#17469=PRODUCT_CONTEXT('part definition',#17468,'mechanical');
#17519=PRODUCT('Output collar (1)','Output collar (1)','Output collar (1)',(#17469));
#17599=COLOUR_RGB('Off White',0.89,0.88,0.83);
#17600=FILL_AREA_STYLE_COLOUR('',#17599);
#17601=FILL_AREA_STYLE('',(#17600));
#17602=SURFACE_STYLE_FILL_AREA(#17601);
#17603=SURFACE_SIDE_STYLE('',(#17602));
#17604=SURFACE_STYLE_USAGE(.BOTH.,#17603);
#17605=PRESENTATION_STYLE_ASSIGNMENT((#17604));
ENDSEC;
END-ISO-10303-21;
